ISO-10303-21;
HEADER;
FILE_DESCRIPTION (('STEP AP214'),
    '1' );
FILE_NAME ('slotted pan head screw_iso_ISO 1580 - M2 x 6 - 6N.step',
    '2026-10-27T04:40:18',
    ( '' ),
    ( '' ),
    'SwSTEP 2.0',
    'SolidWorks 2026',
    '' );
FILE_SCHEMA (( 'AUTOMOTIVE_DESIGN' ));
ENDSEC;

DATA;
#9=CARTESIAN_POINT ( 'NONE',  ( 0.5000000000000000000, 0.2499999999999982792, -1.911797424705720339 ) ) ;
#24=VERTEX_POINT ( 'NONE', #10006 ) ;
#38=AXIS2_PLACEMENT_3D ( 'NONE', #7635, #10225, #6696 ) ;
#50=AXIS2_PLACEMENT_3D ( 'NONE', #1912, #8752, #7861 ) ;
#57=EDGE_CURVE ( 'NONE', #2237, #10334, #9260, .T. ) ;
#88=DIRECTION ( 'NONE',  ( -0.000000000000000000, 1.000000000000000000, 1.224646799147353207E-16 ) ) ;
#89=ORIENTED_EDGE ( 'NONE', *, *, #6443, .F. ) ;
#107=EDGE_CURVE ( 'NONE', #8110, #4251, #4105, .T. ) ;
#142=ORIENTED_EDGE ( 'NONE', *, *, #7024, .F. ) ;
#154=VECTOR ( 'NONE', #5685, 1000.000000000000000 ) ;
#158=FACE_OUTER_BOUND ( 'NONE', #3006, .T. ) ;
#176=PRODUCT_DEFINITION_FORMATION_WITH_SPECIFIED_SOURCE ( 'ANY', '', #2270, .NOT_KNOWN. ) ;
#197=ADVANCED_FACE ( 'NONE', ( #5899 ), #8198, .T. ) ;
#200=AXIS2_PLACEMENT_3D ( 'NONE', #7285, #4873, #3159 ) ;
#213=CARTESIAN_POINT ( 'NONE',  ( 0.5000000000000000000, -0.2499999999999997780, -1.911797424705720116 ) ) ;
#270=CARTESIAN_POINT ( 'NONE',  ( 0.000000000000000000, -0.2499999999999998335, -1.312875263449798879 ) ) ;
#282=ORIENTED_EDGE ( 'NONE', *, *, #3450, .T. ) ;
#302=VERTEX_POINT ( 'NONE', #9 ) ;
#333=DIRECTION ( 'NONE',  ( 0.9961946980917455452, 0.000000000000000000, -0.08715574274765848506 ) ) ;
#345=CARTESIAN_POINT ( 'NONE',  ( 0.6000000000000000888, 0.000000000000000000, 1.336466033005844434 ) ) ;
#364=EDGE_LOOP ( 'NONE', ( #89, #5630 ) ) ;
#367=EDGE_CURVE ( 'NONE', #1845, #302, #9832, .T. ) ;
#410=VECTOR ( 'NONE', #7808, 1000.000000000000000 ) ;
#465=CARTESIAN_POINT ( 'NONE',  ( 7.300000000000000711, 0.000000000000000000, 0.000000000000000000 ) ) ;
#474=SHAPE_DEFINITION_REPRESENTATION ( #8222, #2752 ) ;
#534=EDGE_LOOP ( 'NONE', ( #1368, #8462, #4338, #10886 ) ) ;
#553=CARTESIAN_POINT ( 'NONE',  ( 0.000000000000000000, 0.2499999999999982792, 2.000000000000001776 ) ) ;
#554=ORIENTED_EDGE ( 'NONE', *, *, #5299, .F. ) ;
#555=EDGE_CURVE ( 'NONE', #9700, #1702, #8379, .T. ) ;
#600=CIRCLE ( 'NONE', #9605, 1.928074011315806136 ) ;
#614=ADVANCED_FACE ( 'NONE', ( #3275 ), #4286, .T. ) ;
#629=CARTESIAN_POINT ( 'NONE',  ( 7.300000000000000711, 0.000000000000000000, 0.000000000000000000 ) ) ;
#656=FACE_OUTER_BOUND ( 'NONE', #364, .T. ) ;
#666=ORIENTED_EDGE ( 'NONE', *, *, #6256, .F. ) ;
#677=EDGE_CURVE ( 'NONE', #24, #3356, #3404, .T. ) ;
#696=FACE_OUTER_BOUND ( 'NONE', #8472, .T. ) ;
#698=FILL_AREA_STYLE_COLOUR ( '', #3359 ) ;
#701=( NAMED_UNIT ( * ) SI_UNIT ( $, .STERADIAN. ) SOLID_ANGLE_UNIT ( ) );
#753=CIRCLE ( 'NONE', #921, 2.000000000000000000 ) ;
#770=CIRCLE ( 'NONE', #9120, 1.000000000000000000 ) ;
#774=CARTESIAN_POINT ( 'NONE',  ( 0.6000000000000000888, 0.000000000000000000, 0.000000000000000000 ) ) ;
#813=CARTESIAN_POINT ( 'NONE',  ( 0.000000000000000000, 0.2499999999999982792, 1.312875263449799323 ) ) ;
#816=ORIENTED_EDGE ( 'NONE', *, *, #555, .F. ) ;
#825=DIRECTION ( 'NONE',  ( -0.000000000000000000, 0.000000000000000000, 1.000000000000000000 ) ) ;
#840=DIRECTION ( 'NONE',  ( 1.000000000000000000, 0.000000000000000000, 0.000000000000000000 ) ) ;
#921=AXIS2_PLACEMENT_3D ( 'NONE', #4939, #10835, #4055 ) ;
#946=CARTESIAN_POINT ( 'NONE',  ( -1.470152734901925752E-14, 0.2499999999999982792, -1.453737367178236983 ) ) ;
#980=ADVANCED_FACE ( 'NONE', ( #3711 ), #7111, .F. ) ;
#1021=DIRECTION ( 'NONE',  ( 1.000000000000000000, 0.000000000000000000, 0.000000000000000000 ) ) ;
#1078=ORIENTED_EDGE ( 'NONE', *, *, #5299, .T. ) ;
#1096=MANIFOLD_SOLID_BREP ( 'Slot', #8918 ) ;
#1149=CARTESIAN_POINT ( 'NONE',  ( 1.299999999999999156, 0.000000000000000000, 0.000000000000000000 ) ) ;
#1184=ORIENTED_EDGE ( 'NONE', *, *, #3450, .F. ) ;
#1271=CARTESIAN_POINT ( 'NONE',  ( -9.262305278225771052E-15, -0.2499999999999999445, 1.454152683131084256 ) ) ;
#1288=EDGE_CURVE ( 'NONE', #5990, #4251, #8584, .T. ) ;
#1291=CARTESIAN_POINT ( 'NONE',  ( 0.5000000000000000000, -0.2499999999999997780, -2.000000000000000000 ) ) ;
#1335=ORIENTED_EDGE ( 'NONE', *, *, #5192, .T. ) ;
#1368=ORIENTED_EDGE ( 'NONE', *, *, #367, .T. ) ;
#1451=CARTESIAN_POINT ( 'NONE',  ( 0.5477065543514070267, 0.000000000000000000, 0.000000000000000000 ) ) ;
#1486=CIRCLE ( 'NONE', #8392, 1.928074011315806136 ) ;
#1494=CARTESIAN_POINT ( 'NONE',  ( 1.314929834301322591E-16, 0.000000000000000000, 0.000000000000000000 ) ) ;
#1497=PLANE ( 'NONE',  #200 ) ;
#1511=DIRECTION ( 'NONE',  ( 0.000000000000000000, 0.000000000000000000, 1.000000000000000000 ) ) ;
#1536=ORIENTED_EDGE ( 'NONE', *, *, #5232, .F. ) ;
#1654=CARTESIAN_POINT ( 'NONE',  ( 0.000000000000000000, -0.2499999999999997780, -2.000000000000000000 ) ) ;
#1674=CARTESIAN_POINT ( 'NONE',  ( 0.000000000000000000, 2.310008073021392480E-16, 1.886264737416298409 ) ) ;
#1693=EDGE_LOOP ( 'NONE', ( #9838, #1184 ) ) ;
#1702=VERTEX_POINT ( 'NONE', #6904 ) ;
#1706=DIRECTION ( 'NONE',  ( 1.000000000000000000, 0.000000000000000000, 0.000000000000000000 ) ) ;
#1711=CARTESIAN_POINT ( 'NONE',  ( 0.5000000000000000000, -0.2499999999999997780, -1.911797424705720116 ) ) ;
#1726=CARTESIAN_POINT ( 'NONE',  ( 7.300000000000000711, 1.224646799147353207E-16, -1.000000000000000000 ) ) ;
#1794=FACE_OUTER_BOUND ( 'NONE', #534, .T. ) ;
#1807=EDGE_CURVE ( 'NONE', #24, #8835, #9112, .T. ) ;
#1821=CONICAL_SURFACE ( 'NONE', #7325, 1.886264737416298409, 0.08726646259971679309 ) ;
#1822=ORIENTED_EDGE ( 'NONE', *, *, #9409, .T. ) ;
#1844=CARTESIAN_POINT ( 'NONE',  ( 0.2300425840023382074, 0.2499999999999982236, -1.812072026511089229 ) ) ;
#1845=VERTEX_POINT ( 'NONE', #8186 ) ;
#1897=CARTESIAN_POINT ( 'NONE',  ( 0.5000000000000000000, 0.2499999999999982792, -1.911797424705720339 ) ) ;
#1905=EDGE_LOOP ( 'NONE', ( #4834, #2718, #1984, #3668 ) ) ;
#1912=CARTESIAN_POINT ( 'NONE',  ( 0.000000000000000000, 0.000000000000000000, 0.000000000000000000 ) ) ;
#1946=CARTESIAN_POINT ( 'NONE',  ( 0.000000000000000000, 0.000000000000000000, -1.886264737416298409 ) ) ;
#1955=EDGE_CURVE ( 'NONE', #9681, #1845, #7340, .T. ) ;
#1967=( LENGTH_UNIT ( ) NAMED_UNIT ( * ) SI_UNIT ( .MILLI., .METRE. ) );
#1984=ORIENTED_EDGE ( 'NONE', *, *, #6612, .F. ) ;
#2017=AXIS2_PLACEMENT_3D ( 'NONE', #3794, #7184, #10618 ) ;
#2132=ADVANCED_FACE ( 'NONE', ( #3460 ), #6275, .T. ) ;
#2143=EDGE_CURVE ( 'NONE', #9954, #8835, #1486, .T. ) ;
#2184=DIRECTION ( 'NONE',  ( 1.000000000000000000, -0.000000000000000000, -0.000000000000000000 ) ) ;
#2215=CARTESIAN_POINT ( 'NONE',  ( 0.5000000000000000000, 0.000000000000000000, 0.000000000000000000 ) ) ;
#2237=VERTEX_POINT ( 'NONE', #3808 ) ;
#2263=DIRECTION ( 'NONE',  ( 1.000000000000000000, -0.000000000000000000, -0.000000000000000000 ) ) ;
#2265=CARTESIAN_POINT ( 'NONE',  ( 1.314929834301322591E-16, 0.000000000000000000, 0.000000000000000000 ) ) ;
#2270=PRODUCT ( 'slotted pan head screw_iso_ISO 1580 - M2 x 6 - 6N', 'slotted pan head screw_iso_ISO 1580 - M2 x 6 - 6N', '', ( #2861 ) ) ;
#2289=AXIS2_PLACEMENT_3D ( 'NONE', #6388, #4032, #5542 ) ;
#2290=ORIENTED_EDGE ( 'NONE', *, *, #57, .F. ) ;
#2307=AXIS2_PLACEMENT_3D ( 'NONE', #5193, #3646, #1706 ) ;
#2333=DIRECTION ( 'NONE',  ( 0.000000000000000000, -5.421010862427519705E-17, 1.000000000000000000 ) ) ;
#2350=ORIENTED_EDGE ( 'NONE', *, *, #5232, .T. ) ;
#2358=DIRECTION ( 'NONE',  ( 1.000000000000000000, -0.000000000000000000, -0.000000000000000000 ) ) ;
#2420=DIRECTION ( 'NONE',  ( 0.000000000000000000, -1.224646799147352961E-16, 1.000000000000000000 ) ) ;
#2421=ORIENTED_EDGE ( 'NONE', *, *, #3578, .T. ) ;
#2468=SURFACE_SIDE_STYLE ('',( #7531 ) ) ;
#2476=AXIS2_PLACEMENT_3D ( 'NONE', #1494, #6503, #3105 ) ;
#2481=PRODUCT_DEFINITION_CONTEXT ( 'detailed design', #6495, 'design' ) ;
#2483=CARTESIAN_POINT ( 'NONE',  ( 0.2309188673393134938, 0.2499999999999982792, 1.812888087824517713 ) ) ;
#2487=EDGE_CURVE ( 'NONE', #5990, #5765, #770, .T. ) ;
#2525=STYLED_ITEM('',(#11027),#1096);
#2547=ADVANCED_FACE ( 'NONE', ( #6835 ), #8663, .T. ) ;
#2602=FACE_BOUND ( 'NONE', #6294, .T. ) ;
#2634=EDGE_LOOP ( 'NONE', ( #3642, #3317 ) ) ;
#2636=CIRCLE ( 'NONE', #3165, 2.000000000000000000 ) ;
#2653=ORIENTED_EDGE ( 'NONE', *, *, #677, .F. ) ;
#2681=CARTESIAN_POINT ( 'NONE',  ( 0.5477065543514070267, 0.000000000000000000, 0.000000000000000000 ) ) ;
#2710=CIRCLE ( 'NONE', #7852, 1.000000000000000000 ) ;
#2718=ORIENTED_EDGE ( 'NONE', *, *, #5610, .T. ) ;
#2752=SHAPE_REPRESENTATION ( 'slotted pan head screw_iso_ISO 1580 - M2 x 6 - 6N', ( #2307 ), #4612 ) ;
#2778=LINE ( 'NONE', #1946, #10799 ) ;
#2805=CARTESIAN_POINT ( 'NONE',  ( -25.39999999999996305, 0.000000000000000000, 1.000000000000000000 ) ) ;
#2811=ORIENTED_EDGE ( 'NONE', *, *, #3578, .F. ) ;
#2861=PRODUCT_CONTEXT ( 'NONE', #10669, 'mechanical' ) ;
#2882=DIRECTION ( 'NONE',  ( 0.000000000000000000, 0.000000000000000000, -1.000000000000000000 ) ) ;
#2898=LINE ( 'NONE', #10610, #7430 ) ;
#2962=ORIENTED_EDGE ( 'NONE', *, *, #8420, .F. ) ;
#3006=EDGE_LOOP ( 'NONE', ( #554, #2811 ) ) ;
#3049=CARTESIAN_POINT ( 'NONE',  ( 0.05007909176323187272, -0.2500000000000000000, 1.595164775286565861 ) ) ;
#3052=FACE_OUTER_BOUND ( 'NONE', #10804, .T. ) ;
#3103=CARTESIAN_POINT ( 'NONE',  ( 0.5000000000000000000, 0.2499999999999982792, 1.911797424705720339 ) ) ;
#3105=DIRECTION ( 'NONE',  ( -0.000000000000000000, 0.000000000000000000, 1.000000000000000000 ) ) ;
#3106=ADVANCED_FACE ( 'NONE', ( #4642 ), #1821, .T. ) ;
#3159=DIRECTION ( 'NONE',  ( 0.000000000000000000, 0.000000000000000000, -1.000000000000000000 ) ) ;
#3165=AXIS2_PLACEMENT_3D ( 'NONE', #5496, #10498, #10557 ) ;
#3184=DIRECTION ( 'NONE',  ( -1.000000000000000000, -0.000000000000000000, -0.000000000000000000 ) ) ;
#3248=SURFACE_STYLE_USAGE ( .BOTH. , #2468 ) ;
#3249=AXIS2_PLACEMENT_3D ( 'NONE', #345, #8964, #9795 ) ;
#3254=AXIS2_PLACEMENT_3D ( 'NONE', #8554, #10436, #9493 ) ;
#3264=B_SPLINE_CURVE_WITH_KNOTS ( 'NONE', 3,
 ( #213, #3599, #6160, #4486, #7892, #270 ),
 .UNSPECIFIED., .F., .F.,
 ( 4, 2, 4 ),
 ( 0.003549988921687060456, 0.003971677118101641160, 0.004393365314516220997 ),
 .UNSPECIFIED. ) ;
#3275=FACE_OUTER_BOUND ( 'NONE', #7656, .T. ) ;
#3316=AXIS2_PLACEMENT_3D ( 'NONE', #2265, #5863, #5648 ) ;
#3317=ORIENTED_EDGE ( 'NONE', *, *, #1955, .T. ) ;
#3321=DIRECTION ( 'NONE',  ( 0.000000000000000000, 0.000000000000000000, 1.000000000000000000 ) ) ;
#3336=DIRECTION ( 'NONE',  ( 0.000000000000000000, 0.000000000000000000, 1.000000000000000000 ) ) ;
#3356=VERTEX_POINT ( 'NONE', #5749 ) ;
#3359=COLOUR_RGB ( '',1.000000000000000000, 0.9490196078431372140, 0.9098039215686274384 ) ;
#3373=ADVANCED_FACE ( 'NONE', ( #696 ), #9810, .T. ) ;
#3376=ORIENTED_EDGE ( 'NONE', *, *, #5610, .F. ) ;
#3395=CARTESIAN_POINT ( 'NONE',  ( 0.5000000000000000000, 0.2499999999999982792, 2.000000000000001776 ) ) ;
#3404=CIRCLE ( 'NONE', #4651, 1.934182851860892116 ) ;
#3450=EDGE_CURVE ( 'NONE', #5765, #5990, #2710, .T. ) ;
#3460=FACE_OUTER_BOUND ( 'NONE', #7210, .T. ) ;
#3508=ORIENTED_EDGE ( 'NONE', *, *, #1955, .F. ) ;
#3514=CARTESIAN_POINT ( 'NONE',  ( 0.5000000000000000000, 0.000000000000000000, 0.000000000000000000 ) ) ;
#3549=LINE ( 'NONE', #1674, #5470 ) ;
#3566=SHAPE_REPRESENTATION_RELATIONSHIP ( 'NONE' , 'NONE' ,  #2752, #10920 ) ;
#3569=DIRECTION ( 'NONE',  ( 1.000000000000000000, -0.000000000000000000, -0.000000000000000000 ) ) ;
#3578=EDGE_CURVE ( 'NONE', #7065, #8335, #753, .T. ) ;
#3599=CARTESIAN_POINT ( 'NONE',  ( 0.3612935698783896754, -0.2499999999999997224, -1.888152147991466245 ) ) ;
#3642=ORIENTED_EDGE ( 'NONE', *, *, #8401, .F. ) ;
#3646=DIRECTION ( 'NONE',  ( 0.000000000000000000, 0.000000000000000000, 1.000000000000000000 ) ) ;
#3668=ORIENTED_EDGE ( 'NONE', *, *, #1288, .F. ) ;
#3703=CARTESIAN_POINT ( 'NONE',  ( 0.5000000000000000000, -0.2500000000000000000, 1.911797424705720116 ) ) ;
#3711=FACE_OUTER_BOUND ( 'NONE', #9027, .T. ) ;
#3719=AXIS2_PLACEMENT_3D ( 'NONE', #6046, #5088, #825 ) ;
#3755=DIRECTION ( 'NONE',  ( 0.000000000000000000, 0.000000000000000000, -1.000000000000000000 ) ) ;
#3794=CARTESIAN_POINT ( 'NONE',  ( 1.084202172485504434E-16, 0.000000000000000000, 0.000000000000000000 ) ) ;
#3808=CARTESIAN_POINT ( 'NONE',  ( 0.000000000000000000, -0.2499999999999998335, -1.312875263449798879 ) ) ;
#3842=LINE ( 'NONE', #1291, #10970 ) ;
#3864=VERTEX_POINT ( 'NONE', #4260 ) ;
#3948=MECHANICAL_DESIGN_GEOMETRIC_PRESENTATION_REPRESENTATION('',(#2525),#6614);
#3992=ORIENTED_EDGE ( 'NONE', *, *, #107, .T. ) ;
#4015=DIRECTION ( 'NONE',  ( 0.000000000000000000, 0.000000000000000000, 1.000000000000000000 ) ) ;
#4032=DIRECTION ( 'NONE',  ( -1.000000000000000000, 0.000000000000000000, 0.000000000000000000 ) ) ;
#4050=ORIENTED_EDGE ( 'NONE', *, *, #7024, .T. ) ;
#4055=DIRECTION ( 'NONE',  ( 0.000000000000000000, 0.000000000000000000, 1.000000000000000000 ) ) ;
#4056=ADVANCED_FACE ( 'NONE', ( #5710 ), #1497, .T. ) ;
#4067=DIRECTION ( 'NONE',  ( -1.000000000000000000, -0.000000000000000000, -0.000000000000000000 ) ) ;
#4081=FILL_AREA_STYLE ('',( #698 ) ) ;
#4105=CIRCLE ( 'NONE', #6779, 1.000000000000000000 ) ;
#4251=VERTEX_POINT ( 'NONE', #7031 ) ;
#4260=CARTESIAN_POINT ( 'NONE',  ( 0.5000000000000000000, -0.2500000000000000000, 1.911797424705720116 ) ) ;
#4286=TOROIDAL_SURFACE ( 'NONE', #8037, 1.336466033005844434, 0.5999999999999999778 ) ;
#4325=CARTESIAN_POINT ( 'NONE',  ( 0.3608130681495591019, 0.2499999999999982792, -1.888070236890895703 ) ) ;
#4338=ORIENTED_EDGE ( 'NONE', *, *, #6256, .T. ) ;
#4475=DIRECTION ( 'NONE',  ( -1.000000000000000000, -0.000000000000000000, -0.000000000000000000 ) ) ;
#4486=CARTESIAN_POINT ( 'NONE',  ( 0.04978537780227577231, -0.2499999999999997224, -1.594765474869573874 ) ) ;
#4530=DIRECTION ( 'NONE',  ( 0.000000000000000000, 0.000000000000000000, 1.000000000000000000 ) ) ;
#4594=EDGE_CURVE ( 'NONE', #1702, #302, #600, .T. ) ;
#4612=( GEOMETRIC_REPRESENTATION_CONTEXT ( 3 ) GLOBAL_UNCERTAINTY_ASSIGNED_CONTEXT ( ( #9944 ) ) GLOBAL_UNIT_ASSIGNED_CONTEXT ( ( #9927, #7481, #9144 ) ) REPRESENTATION_CONTEXT ( 'NONE', 'WORKASPACE' ) );
#4642=FACE_OUTER_BOUND ( 'NONE', #8084, .T. ) ;
#4651=AXIS2_PLACEMENT_3D ( 'NONE', #1451, #4986, #3321 ) ;
#4738=ADVANCED_FACE ( 'NONE', ( #1794 ), #5331, .F. ) ;
#4755=LINE ( 'NONE', #553, #6700 ) ;
#4817=ORIENTED_EDGE ( 'NONE', *, *, #6168, .T. ) ;
#4834=ORIENTED_EDGE ( 'NONE', *, *, #2487, .T. ) ;
#4855=ORIENTED_EDGE ( 'NONE', *, *, #1807, .T. ) ;
#4873=DIRECTION ( 'NONE',  ( 1.000000000000000000, 0.000000000000000000, 0.000000000000000000 ) ) ;
#4922=PLANE ( 'NONE',  #2476 ) ;
#4939=CARTESIAN_POINT ( 'NONE',  ( 1.299999999999999156, 0.000000000000000000, 0.000000000000000000 ) ) ;
#4951=LINE ( 'NONE', #9024, #154 ) ;
#4982=ORIENTED_EDGE ( 'NONE', *, *, #1807, .F. ) ;
#4986=DIRECTION ( 'NONE',  ( 1.000000000000000000, 0.000000000000000000, 0.000000000000000000 ) ) ;
#5020=ORIENTED_EDGE ( 'NONE', *, *, #677, .T. ) ;
#5028=LINE ( 'NONE', #1654, #8164 ) ;
#5088=DIRECTION ( 'NONE',  ( -1.000000000000000000, 0.000000000000000000, -0.000000000000000000 ) ) ;
#5192=EDGE_CURVE ( 'NONE', #24, #7065, #3549, .T. ) ;
#5193=CARTESIAN_POINT ( 'NONE',  ( 0.000000000000000000, 0.000000000000000000, 0.000000000000000000 ) ) ;
#5232=EDGE_CURVE ( 'NONE', #3356, #8335, #2778, .T. ) ;
#5240=CARTESIAN_POINT ( 'NONE',  ( 0.000000000000000000, -0.2499999999999999445, 1.312875263449798879 ) ) ;
#5267=CARTESIAN_POINT ( 'NONE',  ( 0.05011565059742434380, 0.2499999999999982792, -1.595010514166263382 ) ) ;
#5275=DIRECTION ( 'NONE',  ( 0.000000000000000000, -0.000000000000000000, 1.000000000000000000 ) ) ;
#5294=CIRCLE ( 'NONE', #10636, 1.000000000000000000 ) ;
#5299=EDGE_CURVE ( 'NONE', #8335, #7065, #2636, .T. ) ;
#5328=DIRECTION ( 'NONE',  ( -1.000000000000000000, -0.000000000000000000, -0.000000000000000000 ) ) ;
#5331=PLANE ( 'NONE',  #9085 ) ;
#5470=VECTOR ( 'NONE', #9328, 1000.000000000000000 ) ;
#5489=MECHANICAL_DESIGN_GEOMETRIC_PRESENTATION_REPRESENTATION('',(#10823),#9580);
#5491=UNCERTAINTY_MEASURE_WITH_UNIT (LENGTH_MEASURE( 1.000000000000000082E-05 ), #1967, 'distance_accuracy_value', 'NONE');
#5496=CARTESIAN_POINT ( 'NONE',  ( 1.299999999999999156, 0.000000000000000000, 0.000000000000000000 ) ) ;
#5511=B_SPLINE_CURVE_WITH_KNOTS ( 'NONE', 3,
 ( #9657, #1271, #3049, #8773, #9596, #3703 ),
 .UNSPECIFIED., .F., .F.,
 ( 4, 2, 4 ),
 ( 0.0005861251363949650413, 0.001008091297609326094, 0.001430057458823687363 ),
 .UNSPECIFIED. ) ;
#5542=DIRECTION ( 'NONE',  ( 0.000000000000000000, 0.000000000000000000, 1.000000000000000000 ) ) ;
#5588=ORIENTED_EDGE ( 'NONE', *, *, #6394, .T. ) ;
#5593=DIRECTION ( 'NONE',  ( 0.000000000000000000, 0.000000000000000000, 1.000000000000000000 ) ) ;
#5610=EDGE_CURVE ( 'NONE', #5765, #8110, #4951, .T. ) ;
#5630=ORIENTED_EDGE ( 'NONE', *, *, #57, .T. ) ;
#5648=DIRECTION ( 'NONE',  ( -0.000000000000000000, 0.000000000000000000, 1.000000000000000000 ) ) ;
#5685=DIRECTION ( 'NONE',  ( -1.000000000000000000, -0.000000000000000000, -0.000000000000000000 ) ) ;
#5710=FACE_OUTER_BOUND ( 'NONE', #1693, .T. ) ;
#5749=CARTESIAN_POINT ( 'NONE',  ( 0.5477065543514070267, 0.000000000000000000, -1.934182851860892116 ) ) ;
#5765=VERTEX_POINT ( 'NONE', #1726 ) ;
#5847=CIRCLE ( 'NONE', #7272, 1.934182851860892116 ) ;
#5863=DIRECTION ( 'NONE',  ( -1.000000000000000000, 0.000000000000000000, -0.000000000000000000 ) ) ;
#5899=FACE_OUTER_BOUND ( 'NONE', #1905, .T. ) ;
#5908=DIRECTION ( 'NONE',  ( 0.000000000000000000, 0.000000000000000000, 1.000000000000000000 ) ) ;
#5920=ORIENTED_EDGE ( 'NONE', *, *, #367, .F. ) ;
#5990=VERTEX_POINT ( 'NONE', #10331 ) ;
#6036=ORIENTED_EDGE ( 'NONE', *, *, #6612, .T. ) ;
#6046=CARTESIAN_POINT ( 'NONE',  ( 1.299999999999999600, 1.000000000000000000, 0.000000000000000000 ) ) ;
#6075=DIRECTION ( 'NONE',  ( 0.000000000000000000, -3.552713678800500929E-15, 1.000000000000000000 ) ) ;
#6110=DIRECTION ( 'NONE',  ( 0.000000000000000000, 0.000000000000000000, -1.000000000000000000 ) ) ;
#6160=CARTESIAN_POINT ( 'NONE',  ( 0.2309054577385447060, -0.2499999999999997780, -1.812959136724909159 ) ) ;
#6168=EDGE_CURVE ( 'NONE', #9700, #3864, #3842, .T. ) ;
#6256=EDGE_CURVE ( 'NONE', #9954, #9681, #6999, .T. ) ;
#6264=AXIS2_PLACEMENT_3D ( 'NONE', #8832, #10600, #8720 ) ;
#6275=CONICAL_SURFACE ( 'NONE', #50, 1.886264737416298409, 0.08726646259971679309 ) ;
#6294=EDGE_LOOP ( 'NONE', ( #6036, #3992 ) ) ;
#6388=CARTESIAN_POINT ( 'NONE',  ( 0.5000000000000000000, 0.2499999999999982792, -2.000000000000000000 ) ) ;
#6394=EDGE_CURVE ( 'NONE', #3356, #1702, #6568, .T. ) ;
#6443=EDGE_CURVE ( 'NONE', #2237, #10334, #5028, .T. ) ;
#6495=APPLICATION_CONTEXT ( 'automotive_design' ) ;
#6500=PLANE ( 'NONE',  #2289 ) ;
#6503=DIRECTION ( 'NONE',  ( -1.000000000000000000, 0.000000000000000000, -0.000000000000000000 ) ) ;
#6511=UNCERTAINTY_MEASURE_WITH_UNIT (LENGTH_MEASURE( 1.000000000000000082E-05 ), #10126, 'distance_accuracy_value', 'NONE');
#6558=ORIENTED_EDGE ( 'NONE', *, *, #6168, .F. ) ;
#6568=CIRCLE ( 'NONE', #7448, 0.5999999999999999778 ) ;
#6612=EDGE_CURVE ( 'NONE', #4251, #8110, #5294, .T. ) ;
#6614=( GEOMETRIC_REPRESENTATION_CONTEXT ( 3 ) GLOBAL_UNCERTAINTY_ASSIGNED_CONTEXT ( ( #6511 ) ) GLOBAL_UNIT_ASSIGNED_CONTEXT ( ( #10126, #6811, #701 ) ) REPRESENTATION_CONTEXT ( 'NONE', 'WORKASPACE' ) );
#6652=PRESENTATION_STYLE_ASSIGNMENT (( #3248 ) ) ;
#6661=CARTESIAN_POINT ( 'NONE',  ( 0.6000000000000000888, 1.636698849489768475E-16, -1.336466033005844434 ) ) ;
#6696=DIRECTION ( 'NONE',  ( 0.000000000000000000, 0.000000000000000000, 1.000000000000000000 ) ) ;
#6700=VECTOR ( 'NONE', #2882, 1000.000000000000000 ) ;
#6710=CARTESIAN_POINT ( 'NONE',  ( 1.299999999999999156, 1.224646799147353207E-16, -1.000000000000000000 ) ) ;
#6774=CARTESIAN_POINT ( 'NONE',  ( 0.000000000000000000, 0.2499999999999982792, 1.312875263449799323 ) ) ;
#6779=AXIS2_PLACEMENT_3D ( 'NONE', #9132, #8406, #4015 ) ;
#6811=( NAMED_UNIT ( * ) PLANE_ANGLE_UNIT ( ) SI_UNIT ( $, .RADIAN. ) );
#6835=FACE_OUTER_BOUND ( 'NONE', #9420, .T. ) ;
#6852=DIRECTION ( 'NONE',  ( 0.000000000000000000, 1.000000000000000000, 0.000000000000000000 ) ) ;
#6904=CARTESIAN_POINT ( 'NONE',  ( 0.5000000000000000000, 2.361209666477099964E-16, -1.928074011315806136 ) ) ;
#6999=B_SPLINE_CURVE_WITH_KNOTS ( 'NONE', 3,
 ( #3103, #9939, #2483, #8318, #8480, #813 ),
 .UNSPECIFIED., .F., .F.,
 ( 4, 2, 4 ),
 ( 0.002363858439908544419, 0.002786031303543298580, 0.003208204167178053175 ),
 .UNSPECIFIED. ) ;
#7024=EDGE_CURVE ( 'NONE', #3356, #24, #5847, .T. ) ;
#7031=CARTESIAN_POINT ( 'NONE',  ( 1.299999999999999156, 0.000000000000000000, 1.000000000000000000 ) ) ;
#7065=VERTEX_POINT ( 'NONE', #10391 ) ;
#7111=PLANE ( 'NONE',  #6264 ) ;
#7184=DIRECTION ( 'NONE',  ( -1.000000000000000000, -0.000000000000000000, -0.000000000000000000 ) ) ;
#7210=EDGE_LOOP ( 'NONE', ( #10957, #5020, #2350, #1078 ) ) ;
#7238=AXIS2_PLACEMENT_3D ( 'NONE', #2215, #2263, #5593 ) ;
#7272=AXIS2_PLACEMENT_3D ( 'NONE', #2681, #840, #8455 ) ;
#7285=CARTESIAN_POINT ( 'NONE',  ( 7.299999999999999822, 1.000000000000000000, 0.000000000000000000 ) ) ;
#7320=CARTESIAN_POINT ( 'NONE',  ( 1.299999999999999156, 0.000000000000000000, -2.000000000000000000 ) ) ;
#7325=AXIS2_PLACEMENT_3D ( 'NONE', #9472, #1021, #3755 ) ;
#7340=CIRCLE ( 'NONE', #2017, 1.336466033005844434 ) ;
#7430=VECTOR ( 'NONE', #6110, 1000.000000000000000 ) ;
#7448=AXIS2_PLACEMENT_3D ( 'NONE', #6661, #88, #2420 ) ;
#7481=( NAMED_UNIT ( * ) PLANE_ANGLE_UNIT ( ) SI_UNIT ( $, .RADIAN. ) );
#7498=ADVANCED_FACE ( 'NONE', ( #158, #2602 ), #8390, .F. ) ;
#7531=SURFACE_STYLE_FILL_AREA ( #4081 ) ;
#7635=CARTESIAN_POINT ( 'NONE',  ( 0.6000000000000000888, 0.000000000000000000, 0.000000000000000000 ) ) ;
#7656=EDGE_LOOP ( 'NONE', ( #10033, #2653, #4855, #10245, #2962, #2290, #9401, #8018 ) ) ;
#7722=EDGE_CURVE ( 'NONE', #9700, #2237, #3264, .T. ) ;
#7762=ADVANCED_FACE ( 'NONE', ( #656 ), #4922, .T. ) ;
#7808=DIRECTION ( 'NONE',  ( -1.000000000000000000, -0.000000000000000000, -0.000000000000000000 ) ) ;
#7852=AXIS2_PLACEMENT_3D ( 'NONE', #465, #5328, #10568 ) ;
#7858=( NAMED_UNIT ( * ) PLANE_ANGLE_UNIT ( ) SI_UNIT ( $, .RADIAN. ) );
#7861=DIRECTION ( 'NONE',  ( 0.000000000000000000, 0.000000000000000000, -1.000000000000000000 ) ) ;
#7892=CARTESIAN_POINT ( 'NONE',  ( 8.300922883092140858E-17, -0.2499999999999997780, -1.455170506525537588 ) ) ;
#7947=ORIENTED_EDGE ( 'NONE', *, *, #1288, .T. ) ;
#8018=ORIENTED_EDGE ( 'NONE', *, *, #555, .T. ) ;
#8037=AXIS2_PLACEMENT_3D ( 'NONE', #774, #10733, #9167 ) ;
#8051=ORIENTED_EDGE ( 'NONE', *, *, #8420, .T. ) ;
#8084=EDGE_LOOP ( 'NONE', ( #4050, #1335, #2421, #1536 ) ) ;
#8110=VERTEX_POINT ( 'NONE', #6710 ) ;
#8164=VECTOR ( 'NONE', #8428, 1000.000000000000000 ) ;
#8186=CARTESIAN_POINT ( 'NONE',  ( 0.000000000000000000, 0.2499999999999982792, -1.312875263449799323 ) ) ;
#8198=CYLINDRICAL_SURFACE ( 'NONE', #8548, 1.000000000000000000 ) ;
#8222=PRODUCT_DEFINITION_SHAPE ( 'NONE', 'NONE',  #10791 ) ;
#8301=CIRCLE ( 'NONE', #7238, 1.928074011315806136 ) ;
#8318=CARTESIAN_POINT ( 'NONE',  ( 0.05007509226404533581, 0.2499999999999982236, 1.595201548406556480 ) ) ;
#8322=EDGE_CURVE ( 'NONE', #8835, #3864, #8301, .T. ) ;
#8335=VERTEX_POINT ( 'NONE', #7320 ) ;
#8379=CIRCLE ( 'NONE', #9432, 1.928074011315806136 ) ;
#8390=PLANE ( 'NONE',  #3719 ) ;
#8392=AXIS2_PLACEMENT_3D ( 'NONE', #3514, #3569, #6075 ) ;
#8401=EDGE_CURVE ( 'NONE', #9681, #1845, #4755, .T. ) ;
#8406=DIRECTION ( 'NONE',  ( -1.000000000000000000, -0.000000000000000000, -0.000000000000000000 ) ) ;
#8420=EDGE_CURVE ( 'NONE', #10334, #3864, #5511, .T. ) ;
#8423=FACE_OUTER_BOUND ( 'NONE', #2634, .T. ) ;
#8428=DIRECTION ( 'NONE',  ( 0.000000000000000000, -5.421010862427519705E-17, 1.000000000000000000 ) ) ;
#8455=DIRECTION ( 'NONE',  ( 0.000000000000000000, 0.000000000000000000, 1.000000000000000000 ) ) ;
#8462=ORIENTED_EDGE ( 'NONE', *, *, #9409, .F. ) ;
#8472=EDGE_LOOP ( 'NONE', ( #142, #5588, #9517, #5920, #3508, #666, #8481, #4982 ) ) ;
#8480=CARTESIAN_POINT ( 'NONE',  ( -5.404070203482436163E-16, 0.2499999999999982792, 1.454823465665887605 ) ) ;
#8481=ORIENTED_EDGE ( 'NONE', *, *, #2143, .T. ) ;
#8522=( NAMED_UNIT ( * ) SI_UNIT ( $, .STERADIAN. ) SOLID_ANGLE_UNIT ( ) );
#8525=ORIENTED_EDGE ( 'NONE', *, *, #2143, .F. ) ;
#8548=AXIS2_PLACEMENT_3D ( 'NONE', #10795, #3184, #9967 ) ;
#8554=CARTESIAN_POINT ( 'NONE',  ( -25.39999999999996305, 0.000000000000000000, 0.000000000000000000 ) ) ;
#8584=LINE ( 'NONE', #2805, #410 ) ;
#8595=ORIENTED_EDGE ( 'NONE', *, *, #6443, .T. ) ;
#8598=ADVANCED_FACE ( 'NONE', ( #8423 ), #9203, .T. ) ;
#8651=ORIENTED_EDGE ( 'NONE', *, *, #8322, .F. ) ;
#8663=CYLINDRICAL_SURFACE ( 'NONE', #3254, 1.000000000000000000 ) ;
#8720=DIRECTION ( 'NONE',  ( 0.000000000000000000, 5.421010862427519705E-17, -1.000000000000000000 ) ) ;
#8733=AXIS2_PLACEMENT_3D ( 'NONE', #10900, #4067, #3336 ) ;
#8752=DIRECTION ( 'NONE',  ( 1.000000000000000000, 0.000000000000000000, 0.000000000000000000 ) ) ;
#8773=CARTESIAN_POINT ( 'NONE',  ( 0.2307700686259116507, -0.2500000000000000000, 1.812750528907549175 ) ) ;
#8832=CARTESIAN_POINT ( 'NONE',  ( 0.5000000000000000000, -0.2499999999999997780, -2.000000000000000000 ) ) ;
#8835=VERTEX_POINT ( 'NONE', #9802 ) ;
#8918=CLOSED_SHELL ( 'NONE', ( #3373, #3106, #197, #8598, #2547, #4056, #7762, #2132, #7498, #614, #4738, #980, #10005 ) ) ;
#8961=DIRECTION ( 'NONE',  ( 0.000000000000000000, 1.065814103640150121E-14, 1.000000000000000000 ) ) ;
#8964=DIRECTION ( 'NONE',  ( 0.000000000000000000, -1.000000000000000000, 0.000000000000000000 ) ) ;
#9024=CARTESIAN_POINT ( 'NONE',  ( -25.39999999999996305, 1.224646799147353207E-16, -1.000000000000000000 ) ) ;
#9027=EDGE_LOOP ( 'NONE', ( #10591, #8595, #8051, #6558 ) ) ;
#9085=AXIS2_PLACEMENT_3D ( 'NONE', #3395, #6852, #5275 ) ;
#9112=CIRCLE ( 'NONE', #3249, 0.5999999999999999778 ) ;
#9120=AXIS2_PLACEMENT_3D ( 'NONE', #629, #9960, #1511 ) ;
#9132=CARTESIAN_POINT ( 'NONE',  ( 1.299999999999999156, 0.000000000000000000, 0.000000000000000000 ) ) ;
#9144=( NAMED_UNIT ( * ) SI_UNIT ( $, .STERADIAN. ) SOLID_ANGLE_UNIT ( ) );
#9167=DIRECTION ( 'NONE',  ( 0.000000000000000000, 0.000000000000000000, 1.000000000000000000 ) ) ;
#9203=PLANE ( 'NONE',  #3316 ) ;
#9260=CIRCLE ( 'NONE', #8733, 1.336466033005844434 ) ;
#9328=DIRECTION ( 'NONE',  ( 0.9961946980917455452, 1.067350013832301058E-17, 0.08715574274765848506 ) ) ;
#9401=ORIENTED_EDGE ( 'NONE', *, *, #7722, .F. ) ;
#9409=EDGE_CURVE ( 'NONE', #9954, #302, #2898, .T. ) ;
#9420=EDGE_LOOP ( 'NONE', ( #3376, #282, #7947, #10761 ) ) ;
#9432=AXIS2_PLACEMENT_3D ( 'NONE', #9791, #2184, #8961 ) ;
#9472=CARTESIAN_POINT ( 'NONE',  ( 0.000000000000000000, 0.000000000000000000, 0.000000000000000000 ) ) ;
#9493=DIRECTION ( 'NONE',  ( 0.000000000000000000, 0.000000000000000000, 1.000000000000000000 ) ) ;
#9517=ORIENTED_EDGE ( 'NONE', *, *, #4594, .T. ) ;
#9580=( GEOMETRIC_REPRESENTATION_CONTEXT ( 3 ) GLOBAL_UNCERTAINTY_ASSIGNED_CONTEXT ( ( #5491 ) ) GLOBAL_UNIT_ASSIGNED_CONTEXT ( ( #1967, #7858, #8522 ) ) REPRESENTATION_CONTEXT ( 'NONE', 'WORKASPACE' ) );
#9596=CARTESIAN_POINT ( 'NONE',  ( 0.3600944671415647891, -0.2500000000000000000, 1.887947737020718941 ) ) ;
#9605=AXIS2_PLACEMENT_3D ( 'NONE', #10119, #2358, #5908 ) ;
#9657=CARTESIAN_POINT ( 'NONE',  ( 0.000000000000000000, -0.2499999999999999445, 1.312875263449798879 ) ) ;
#9681=VERTEX_POINT ( 'NONE', #6774 ) ;
#9700=VERTEX_POINT ( 'NONE', #1711 ) ;
#9730=ORIENTED_EDGE ( 'NONE', *, *, #4594, .F. ) ;
#9791=CARTESIAN_POINT ( 'NONE',  ( 0.5000000000000000000, 0.000000000000000000, 0.000000000000000000 ) ) ;
#9795=DIRECTION ( 'NONE',  ( 0.000000000000000000, 0.000000000000000000, -1.000000000000000000 ) ) ;
#9802=CARTESIAN_POINT ( 'NONE',  ( 0.5000000000000000000, 0.000000000000000000, 1.928074011315806136 ) ) ;
#9810=TOROIDAL_SURFACE ( 'NONE', #38, 1.336466033005844434, 0.5999999999999999778 ) ;
#9832=B_SPLINE_CURVE_WITH_KNOTS ( 'NONE', 3,
 ( #10333, #946, #5267, #1844, #4325, #1897 ),
 .UNSPECIFIED., .F., .F.,
 ( 4, 2, 4 ),
 ( 0.003191392849877886309, 0.003612977948258624256, 0.004034563046639362202 ),
 .UNSPECIFIED. ) ;
#9838=ORIENTED_EDGE ( 'NONE', *, *, #2487, .F. ) ;
#9927=( LENGTH_UNIT ( ) NAMED_UNIT ( * ) SI_UNIT ( .MILLI., .METRE. ) );
#9939=CARTESIAN_POINT ( 'NONE',  ( 0.3609765494018736809, 0.2499999999999982792, 1.888098105530059190 ) ) ;
#9944=UNCERTAINTY_MEASURE_WITH_UNIT (LENGTH_MEASURE( 1.000000000000000082E-05 ), #9927, 'distance_accuracy_value', 'NONE');
#9954=VERTEX_POINT ( 'NONE', #10661 ) ;
#9960=DIRECTION ( 'NONE',  ( -1.000000000000000000, -0.000000000000000000, -0.000000000000000000 ) ) ;
#9967=DIRECTION ( 'NONE',  ( 0.000000000000000000, 0.000000000000000000, 1.000000000000000000 ) ) ;
#10005=ADVANCED_FACE ( 'NONE', ( #3052 ), #6500, .T. ) ;
#10006=CARTESIAN_POINT ( 'NONE',  ( 0.5477065543514070267, 2.408992218395923449E-16, 1.934182851860892116 ) ) ;
#10033=ORIENTED_EDGE ( 'NONE', *, *, #6394, .F. ) ;
#10119=CARTESIAN_POINT ( 'NONE',  ( 0.5000000000000000000, 0.000000000000000000, 0.000000000000000000 ) ) ;
#10126=( LENGTH_UNIT ( ) NAMED_UNIT ( * ) SI_UNIT ( .MILLI., .METRE. ) );
#10225=DIRECTION ( 'NONE',  ( -1.000000000000000000, -0.000000000000000000, -0.000000000000000000 ) ) ;
#10245=ORIENTED_EDGE ( 'NONE', *, *, #8322, .T. ) ;
#10331=CARTESIAN_POINT ( 'NONE',  ( 7.300000000000000711, 0.000000000000000000, 1.000000000000000000 ) ) ;
#10333=CARTESIAN_POINT ( 'NONE',  ( 0.000000000000000000, 0.2499999999999982792, -1.312875263449799323 ) ) ;
#10334=VERTEX_POINT ( 'NONE', #5240 ) ;
#10391=CARTESIAN_POINT ( 'NONE',  ( 1.299999999999999156, 2.449293598294706414E-16, 2.000000000000000000 ) ) ;
#10436=DIRECTION ( 'NONE',  ( -1.000000000000000000, -0.000000000000000000, -0.000000000000000000 ) ) ;
#10498=DIRECTION ( 'NONE',  ( -1.000000000000000000, -0.000000000000000000, -0.000000000000000000 ) ) ;
#10557=DIRECTION ( 'NONE',  ( 0.000000000000000000, 0.000000000000000000, 1.000000000000000000 ) ) ;
#10568=DIRECTION ( 'NONE',  ( 0.000000000000000000, 0.000000000000000000, 1.000000000000000000 ) ) ;
#10591=ORIENTED_EDGE ( 'NONE', *, *, #7722, .T. ) ;
#10600=DIRECTION ( 'NONE',  ( 0.000000000000000000, -1.000000000000000000, -5.421010862427519705E-17 ) ) ;
#10610=CARTESIAN_POINT ( 'NONE',  ( 0.5000000000000000000, 0.2499999999999982792, 2.000000000000001776 ) ) ;
#10618=DIRECTION ( 'NONE',  ( 0.000000000000000000, 0.000000000000000000, 1.000000000000000000 ) ) ;
#10636=AXIS2_PLACEMENT_3D ( 'NONE', #1149, #4475, #4530 ) ;
#10661=CARTESIAN_POINT ( 'NONE',  ( 0.5000000000000000000, 0.2499999999999982792, 1.911797424705720339 ) ) ;
#10669=APPLICATION_CONTEXT ( 'automotive_design' ) ;
#10733=DIRECTION ( 'NONE',  ( -1.000000000000000000, -0.000000000000000000, -0.000000000000000000 ) ) ;
#10761=ORIENTED_EDGE ( 'NONE', *, *, #107, .F. ) ;
#10791=PRODUCT_DEFINITION ( 'UNKNOWN', '', #176, #2481 ) ;
#10795=CARTESIAN_POINT ( 'NONE',  ( -25.39999999999996305, 0.000000000000000000, 0.000000000000000000 ) ) ;
#10799=VECTOR ( 'NONE', #333, 1000.000000000000000 ) ;
#10804=EDGE_LOOP ( 'NONE', ( #4817, #8651, #8525, #1822, #9730, #816 ) ) ;
#10823=STYLED_ITEM ( 'NONE', ( #6652 ), #10920 ) ;
#10835=DIRECTION ( 'NONE',  ( -1.000000000000000000, -0.000000000000000000, -0.000000000000000000 ) ) ;
#10886=ORIENTED_EDGE ( 'NONE', *, *, #8401, .T. ) ;
#10900=CARTESIAN_POINT ( 'NONE',  ( 1.084202172485504434E-16, 0.000000000000000000, 0.000000000000000000 ) ) ;
#10920=ADVANCED_BREP_SHAPE_REPRESENTATION ( '', ( #1096, #2307 ), #4612 ) ;
#10957=ORIENTED_EDGE ( 'NONE', *, *, #5192, .F. ) ;
#10970=VECTOR ( 'NONE', #2333, 1000.000000000000000 ) ;
#11021=COLOUR_RGB('Black',0.12,0.14,0.17);
#11022=FILL_AREA_STYLE_COLOUR('',#11021);
#11023=FILL_AREA_STYLE('',(#11022));
#11024=SURFACE_STYLE_FILL_AREA(#11023);
#11025=SURFACE_SIDE_STYLE('',(#11024));
#11026=SURFACE_STYLE_USAGE(.BOTH.,#11025);
#11027=PRESENTATION_STYLE_ASSIGNMENT((#11026));
ENDSEC;
END-ISO-10303-21;
